ISO-10303-21;
HEADER;
/* Generated by software containing ST-Developer
 * from STEP Tools, Inc. (www.steptools.com) 
 */

FILE_DESCRIPTION(
/* description */ ('Two-link friction support arm'),
/* implementation_level */ '2;1');

FILE_NAME(
/* name */ 'Flat Washer - M5.step',
/* time_stamp */ '2026-10-27T20:01:49-07:00',
/* author */ (''),
/* organization */ (''),
/* preprocessor_version */ 'ST-DEVELOPER v20.2',
/* originating_system */ 'Autodesk Translation Framework v15.17.0.0',
/* authorisation */ '');

FILE_SCHEMA (('AUTOMOTIVE_DESIGN { 1 0 10303 214 3 1 1 }'));
ENDSEC;

DATA;
#10=MECHANICAL_DESIGN_GEOMETRIC_PRESENTATION_REPRESENTATION('',(#198),#5492);
#163=CONICAL_SURFACE('',#3399,0.275,0.785398163397449);
#176=SHAPE_REPRESENTATION_RELATIONSHIP('SRR','None',#5567,#187);
#187=ADVANCED_BREP_SHAPE_REPRESENTATION('',(#209),#5481);
#198=STYLED_ITEM('',(#5708),#209);
#209=MANIFOLD_SOLID_BREP('Body1',#3174);
#225=FACE_BOUND('',#626,.T.);
#226=FACE_BOUND('',#629,.T.);
#319=PLANE('',#3404);
#320=PLANE('',#3408);
#447=FACE_OUTER_BOUND('',#623,.T.);
#448=FACE_OUTER_BOUND('',#624,.T.);
#449=FACE_OUTER_BOUND('',#625,.T.);
#450=FACE_OUTER_BOUND('',#627,.T.);
#451=FACE_OUTER_BOUND('',#628,.T.);
#623=EDGE_LOOP('',(#2552,#2553,#2554,#2555));
#624=EDGE_LOOP('',(#2556,#2557,#2558,#2559));
#625=EDGE_LOOP('',(#2560));
#626=EDGE_LOOP('',(#2561));
#627=EDGE_LOOP('',(#2562,#2563,#2564,#2565));
#628=EDGE_LOOP('',(#2566));
#629=EDGE_LOOP('',(#2567));
#934=LINE('',#4947,#1247);
#935=LINE('',#4951,#1248);
#936=LINE('',#4958,#1249);
#1247=VECTOR('',#3990,0.275);
#1248=VECTOR('',#3995,0.265);
#1249=VECTOR('',#4004,0.5);
#1379=CIRCLE('',#3400,0.285);
#1380=CIRCLE('',#3401,0.265);
#1381=CIRCLE('',#3403,0.265);
#1382=CIRCLE('',#3405,0.5);
#1383=CIRCLE('',#3407,0.5);
#1587=VERTEX_POINT('',#4944);
#1588=VERTEX_POINT('',#4946);
#1589=VERTEX_POINT('',#4950);
#1590=VERTEX_POINT('',#4954);
#1591=VERTEX_POINT('',#4957);
#1930=EDGE_CURVE('',#1587,#1587,#1379,.T.);
#1931=EDGE_CURVE('',#1587,#1588,#934,.T.);
#1932=EDGE_CURVE('',#1588,#1588,#1380,.T.);
#1933=EDGE_CURVE('',#1588,#1589,#935,.T.);
#1934=EDGE_CURVE('',#1589,#1589,#1381,.T.);
#1935=EDGE_CURVE('',#1590,#1590,#1382,.T.);
#1936=EDGE_CURVE('',#1590,#1591,#936,.T.);
#1937=EDGE_CURVE('',#1591,#1591,#1383,.T.);
#2552=ORIENTED_EDGE('',*,*,#1930,.T.);
#2553=ORIENTED_EDGE('',*,*,#1931,.T.);
#2554=ORIENTED_EDGE('',*,*,#1932,.T.);
#2555=ORIENTED_EDGE('',*,*,#1931,.F.);
#2556=ORIENTED_EDGE('',*,*,#1932,.F.);
#2557=ORIENTED_EDGE('',*,*,#1933,.T.);
#2558=ORIENTED_EDGE('',*,*,#1934,.T.);
#2559=ORIENTED_EDGE('',*,*,#1933,.F.);
#2560=ORIENTED_EDGE('',*,*,#1935,.T.);
#2561=ORIENTED_EDGE('',*,*,#1930,.F.);
#2562=ORIENTED_EDGE('',*,*,#1935,.F.);
#2563=ORIENTED_EDGE('',*,*,#1936,.T.);
#2564=ORIENTED_EDGE('',*,*,#1937,.T.);
#2565=ORIENTED_EDGE('',*,*,#1936,.F.);
#2566=ORIENTED_EDGE('',*,*,#1937,.F.);
#2567=ORIENTED_EDGE('',*,*,#1934,.F.);
#2973=CYLINDRICAL_SURFACE('',#3402,0.265);
#2974=CYLINDRICAL_SURFACE('',#3406,0.5);
#3078=ADVANCED_FACE('',(#447),#163,.F.);
#3079=ADVANCED_FACE('',(#448),#2973,.F.);
#3080=ADVANCED_FACE('',(#449,#225),#319,.T.);
#3081=ADVANCED_FACE('',(#450),#2974,.T.);
#3082=ADVANCED_FACE('',(#451,#226),#320,.F.);
#3174=CLOSED_SHELL('',(#3078,#3079,#3080,#3081,#3082));
#3398=AXIS2_PLACEMENT_3D('',#4942,#3984,#3985);
#3399=AXIS2_PLACEMENT_3D('',#4943,#3986,#3987);
#3400=AXIS2_PLACEMENT_3D('',#4945,#3988,#3989);
#3401=AXIS2_PLACEMENT_3D('',#4948,#3991,#3992);
#3402=AXIS2_PLACEMENT_3D('',#4949,#3993,#3994);
#3403=AXIS2_PLACEMENT_3D('',#4952,#3996,#3997);
#3404=AXIS2_PLACEMENT_3D('',#4953,#3998,#3999);
#3405=AXIS2_PLACEMENT_3D('',#4955,#4000,#4001);
#3406=AXIS2_PLACEMENT_3D('',#4956,#4002,#4003);
#3407=AXIS2_PLACEMENT_3D('',#4959,#4005,#4006);
#3408=AXIS2_PLACEMENT_3D('',#4960,#4007,#4008);
#3984=DIRECTION('axis',(0.,0.,1.));
#3985=DIRECTION('refdir',(1.,0.,0.));
#3986=DIRECTION('center_axis',(0.,1.,0.));
#3987=DIRECTION('ref_axis',(1.,0.,0.));
#3988=DIRECTION('center_axis',(0.,1.,0.));
#3989=DIRECTION('ref_axis',(1.,0.,0.));
#3990=DIRECTION('',(0.707106781186548,-0.707106781186547,-8.65956056235494E-17));
#3991=DIRECTION('center_axis',(0.,-1.,0.));
#3992=DIRECTION('ref_axis',(1.,0.,0.));
#3993=DIRECTION('center_axis',(0.,1.,0.));
#3994=DIRECTION('ref_axis',(1.,0.,0.));
#3995=DIRECTION('',(0.,-1.,0.));
#3996=DIRECTION('center_axis',(0.,-1.,0.));
#3997=DIRECTION('ref_axis',(1.,0.,0.));
#3998=DIRECTION('center_axis',(0.,1.,0.));
#3999=DIRECTION('ref_axis',(1.,0.,0.));
#4000=DIRECTION('center_axis',(0.,1.,0.));
#4001=DIRECTION('ref_axis',(1.,0.,0.));
#4002=DIRECTION('center_axis',(0.,1.,0.));
#4003=DIRECTION('ref_axis',(1.,0.,0.));
#4004=DIRECTION('',(0.,-1.,0.));
#4005=DIRECTION('center_axis',(0.,1.,0.));
#4006=DIRECTION('ref_axis',(1.,0.,0.));
#4007=DIRECTION('center_axis',(0.,1.,0.));
#4008=DIRECTION('ref_axis',(1.,0.,0.));
#4942=CARTESIAN_POINT('',(0.,0.,0.));
#4943=CARTESIAN_POINT('Origin',(0.,0.09,0.));
#4944=CARTESIAN_POINT('',(-0.285,0.1,3.49024337756996E-17));
#4945=CARTESIAN_POINT('Origin',(0.,0.1,0.));
#4946=CARTESIAN_POINT('',(-0.265,0.08,-3.24531401774049E-17));
#4947=CARTESIAN_POINT('',(-0.275,0.09,3.36777869765522E-17));
#4948=CARTESIAN_POINT('Origin',(0.,0.08,0.));
#4949=CARTESIAN_POINT('Origin',(0.,0.,0.));
#4950=CARTESIAN_POINT('',(-0.265,0.,3.24531401774049E-17));
#4951=CARTESIAN_POINT('',(-0.265,0.,3.24531401774049E-17));
#4952=CARTESIAN_POINT('Origin',(0.,0.,0.));
#4953=CARTESIAN_POINT('Origin',(0.,0.1,0.));
#4954=CARTESIAN_POINT('',(-0.5,0.1,6.12323399573677E-17));
#4955=CARTESIAN_POINT('Origin',(0.,0.1,0.));
#4956=CARTESIAN_POINT('Origin',(0.,0.,0.));
#4957=CARTESIAN_POINT('',(-0.5,0.,6.12323399573677E-17));
#4958=CARTESIAN_POINT('',(-0.5,0.,6.12323399573677E-17));
#4959=CARTESIAN_POINT('Origin',(0.,0.,0.));
#4960=CARTESIAN_POINT('Origin',(0.,0.,0.));
#5464=UNCERTAINTY_MEASURE_WITH_UNIT(LENGTH_MEASURE(0.001),#5493,
'DISTANCE_ACCURACY_VALUE',
'Maximum model space distance between geometric entities at asserted c
onnectivities');
#5475=UNCERTAINTY_MEASURE_WITH_UNIT(LENGTH_MEASURE(0.001),#5493,
'DISTANCE_ACCURACY_VALUE',
'Maximum model space distance between geometric entities at asserted c
onnectivities');
#5481=(
GEOMETRIC_REPRESENTATION_CONTEXT(3)
GLOBAL_UNCERTAINTY_ASSIGNED_CONTEXT((#5464))
GLOBAL_UNIT_ASSIGNED_CONTEXT((#5493,#5495,#5496))
REPRESENTATION_CONTEXT('','3D')
);
#5492=(
GEOMETRIC_REPRESENTATION_CONTEXT(3)
GLOBAL_UNCERTAINTY_ASSIGNED_CONTEXT((#5475))
GLOBAL_UNIT_ASSIGNED_CONTEXT((#5493,#5495,#5496))
REPRESENTATION_CONTEXT('','3D')
);
#5493=(
LENGTH_UNIT()
NAMED_UNIT(*)
SI_UNIT(.CENTI.,.METRE.)
);
#5495=(
NAMED_UNIT(*)
PLANE_ANGLE_UNIT()
SI_UNIT($,.RADIAN.)
);
#5496=(
NAMED_UNIT(*)
SI_UNIT($,.STERADIAN.)
SOLID_ANGLE_UNIT()
);
#5502=SHAPE_DEFINITION_REPRESENTATION(#5518,#5567);
#5518=PRODUCT_DEFINITION_SHAPE('',$,#5584);
#5567=SHAPE_REPRESENTATION('',(#3398),#5481);
#5578=PRODUCT_DEFINITION_CONTEXT('part definition',#5628,'design');
#5584=PRODUCT_DEFINITION('Flat Washer - M5','Flat Washer - M5',#5600,#5578);
#5600=PRODUCT_DEFINITION_FORMATION('',$,#5635);
#5628=APPLICATION_CONTEXT(
'Core Data for Automotive Mechanical Design Process');
#5629=PRODUCT_CONTEXT('part definition',#5628,'mechanical');
#5635=PRODUCT('Flat Washer - M5','Flat Washer - M5','Flat Washer - M5',
(#5629));
#5702=COLOUR_RGB('Black',0.12,0.14,0.17);
#5703=FILL_AREA_STYLE_COLOUR('',#5702);
#5704=FILL_AREA_STYLE('',(#5703));
#5705=SURFACE_STYLE_FILL_AREA(#5704);
#5706=SURFACE_SIDE_STYLE('',(#5705));
#5707=SURFACE_STYLE_USAGE(.BOTH.,#5706);
#5708=PRESENTATION_STYLE_ASSIGNMENT((#5707));
ENDSEC;
END-ISO-10303-21;
